ISO-10303-21;
HEADER;
FILE_DESCRIPTION (('STEP AP214'),
    '1' );
FILE_NAME ('socket head cap screw_iso_ISO 4762 M5 x 16 - 16N.step',
    '2026-10-08T14:59:03',
    ( '' ),
    ( '' ),
    'SwSTEP 2.0',
    'SolidWorks 2026',
    '' );
FILE_SCHEMA (( 'AUTOMOTIVE_DESIGN' ));
ENDSEC;

DATA;
#30=UNCERTAINTY_MEASURE_WITH_UNIT (LENGTH_MEASURE( 1.000000000000000082E-05 ), #8409, 'distance_accuracy_value', 'NONE');
#66=CARTESIAN_POINT ( 'NONE',  ( 2.500000000000000000, -1.178949249685214307, 2.042000000000001592 ) ) ;
#84=DIRECTION ( 'NONE',  ( 0.000000000000000000, 0.000000000000000000, 1.000000000000000000 ) ) ;
#132=ORIENTED_EDGE ( 'NONE', *, *, #1282, .T. ) ;
#158=AXIS2_PLACEMENT_3D ( 'NONE', #4049, #10649, #3342 ) ;
#185=AXIS2_PLACEMENT_3D ( 'NONE', #6233, #8025, #4294 ) ;
#193=LINE ( 'NONE', #8731, #4891 ) ;
#199=CARTESIAN_POINT ( 'NONE',  ( 5.000000000000000888, 0.000000000000000000, 0.000000000000000000 ) ) ;
#236=DIRECTION ( 'NONE',  ( 0.000000000000000000, -0.5000000000000013323, -0.8660254037844380415 ) ) ;
#259=FACE_OUTER_BOUND ( 'NONE', #8887, .T. ) ;
#260=LINE ( 'NONE', #1697, #8889 ) ;
#272=ORIENTED_EDGE ( 'NONE', *, *, #9842, .T. ) ;
#279=ORIENTED_EDGE ( 'NONE', *, *, #3805, .F. ) ;
#345=CARTESIAN_POINT ( 'NONE',  ( 5.200000000000002842, 0.000000000000000000, -2.700000000000000622 ) ) ;
#354=EDGE_CURVE ( 'NONE', #3011, #4721, #2953, .T. ) ;
#384=VECTOR ( 'NONE', #6845, 1000.000000000000000 ) ;
#402=ORIENTED_EDGE ( 'NONE', *, *, #10964, .T. ) ;
#409=DIRECTION ( 'NONE',  ( 0.000000000000000000, 0.000000000000000000, -1.000000000000000000 ) ) ;
#442=CARTESIAN_POINT ( 'NONE',  ( 2.500000000000000000, 2.357898499370431722, -2.818925648462311528E-15 ) ) ;
#444=DIRECTION ( 'NONE',  ( -0.5000000000000051070, 0.000000000000000000, 0.8660254037844355990 ) ) ;
#448=EDGE_CURVE ( 'NONE', #1030, #9112, #4774, .T. ) ;
#485=ORIENTED_EDGE ( 'NONE', *, *, #3805, .T. ) ;
#490=ORIENTED_EDGE ( 'NONE', *, *, #11919, .F. ) ;
#501=EDGE_LOOP ( 'NONE', ( #8334, #7320, #8092, #12051 ) ) ;
#553=DIRECTION ( 'NONE',  ( 1.000000000000000000, 0.000000000000000000, 0.000000000000000000 ) ) ;
#554=ORIENTED_EDGE ( 'NONE', *, *, #8544, .F. ) ;
#562=ORIENTED_EDGE ( 'NONE', *, *, #11113, .T. ) ;
#568=FACE_OUTER_BOUND ( 'NONE', #8692, .T. ) ;
#607=DIRECTION ( 'NONE',  ( 1.000000000000000000, 0.000000000000000000, 0.000000000000000000 ) ) ;
#639=EDGE_CURVE ( 'NONE', #4325, #2631, #2857, .T. ) ;
#664=CARTESIAN_POINT ( 'NONE',  ( 3.678949249685231848, 0.000000000000000000, 0.000000000000000000 ) ) ;
#743=FACE_BOUND ( 'NONE', #5622, .T. ) ;
#762=( NAMED_UNIT ( * ) SI_UNIT ( $, .STERADIAN. ) SOLID_ANGLE_UNIT ( ) );
#778=SHAPE_REPRESENTATION ( 'socket head cap screw_iso_ISO 4762 M5 x 16 - 16N', ( #1612 ), #6744 ) ;
#780=LINE ( 'NONE', #5636, #5073 ) ;
#801=DIRECTION ( 'NONE',  ( 0.000000000000000000, -0.5000000000000013323, -0.8660254037844380415 ) ) ;
#812=DIRECTION ( 'NONE',  ( -1.000000000000000000, -0.000000000000000000, -0.000000000000000000 ) ) ;
#822=FILL_AREA_STYLE_COLOUR ( '', #4749 ) ;
#825=CARTESIAN_POINT ( 'NONE',  ( 2.500000000000000000, 0.000000000000000000, 0.000000000000000000 ) ) ;
#833=AXIS2_PLACEMENT_3D ( 'NONE', #2685, #5686, #10344 ) ;
#875=VERTEX_POINT ( 'NONE', #5586 ) ;
#903=EDGE_CURVE ( 'NONE', #3768, #6428, #7068, .T. ) ;
#912=ORIENTED_EDGE ( 'NONE', *, *, #11212, .F. ) ;
#936=CIRCLE ( 'NONE', #8681, 0.2500000000000002220 ) ;
#956=EDGE_CURVE ( 'NONE', #3370, #4721, #6850, .T. ) ;
#959=DIRECTION ( 'NONE',  ( -0.7071067811865364705, 8.659560562355067211E-17, -0.7071067811865584529 ) ) ;
#960=DIRECTION ( 'NONE',  ( 0.000000000000000000, 1.000000000000000000, -1.287488025362403787E-15 ) ) ;
#974=CARTESIAN_POINT ( 'NONE',  ( 2.500000000000000000, 2.357898499370431722, -2.818925648462311528E-15 ) ) ;
#976=CARTESIAN_POINT ( 'NONE',  ( 2.500000000000000000, 0.000000000000000000, 0.000000000000000000 ) ) ;
#979=PRODUCT_DEFINITION_FORMATION_WITH_SPECIFIED_SOURCE ( 'ANY', '', #10458, .NOT_KNOWN. ) ;
#987=DIRECTION ( 'NONE',  ( 0.000000000000000000, -0.4999999999999993339, 0.8660254037844390407 ) ) ;
#989=ORIENTED_EDGE ( 'NONE', *, *, #12075, .T. ) ;
#1030=VERTEX_POINT ( 'NONE', #6887 ) ;
#1033=ORIENTED_EDGE ( 'NONE', *, *, #9798, .T. ) ;
#1075=ORIENTED_EDGE ( 'NONE', *, *, #6041, .F. ) ;
#1078=ORIENTED_EDGE ( 'NONE', *, *, #956, .T. ) ;
#1085=DIRECTION ( 'NONE',  ( 0.000000000000000000, -1.000000000000000000, 1.287488025362403787E-15 ) ) ;
#1088=EDGE_LOOP ( 'NONE', ( #4002, #7356 ) ) ;
#1096=DIRECTION ( 'NONE',  ( -1.000000000000000000, -0.000000000000000000, -0.000000000000000000 ) ) ;
#1138=EDGE_CURVE ( 'NONE', #12045, #4325, #2520, .T. ) ;
#1143=DIRECTION ( 'NONE',  ( -0.7071067811865364705, 0.000000000000000000, 0.7071067811865584529 ) ) ;
#1146=DIRECTION ( 'NONE',  ( 0.000000000000000000, 0.000000000000000000, 1.000000000000000000 ) ) ;
#1164=ORIENTED_EDGE ( 'NONE', *, *, #9842, .F. ) ;
#1202=ORIENTED_EDGE ( 'NONE', *, *, #12075, .F. ) ;
#1214=ORIENTED_EDGE ( 'NONE', *, *, #1804, .T. ) ;
#1218=ORIENTED_EDGE ( 'NONE', *, *, #3200, .F. ) ;
#1222=EDGE_CURVE ( 'NONE', #10746, #3370, #3820, .T. ) ;
#1236=VERTEX_POINT ( 'NONE', #1708 ) ;
#1240=EDGE_CURVE ( 'NONE', #1030, #3768, #780, .T. ) ;
#1276=CARTESIAN_POINT ( 'NONE',  ( 2.500000000000000000, 0.000000000000000000, 0.000000000000000000 ) ) ;
#1282=EDGE_CURVE ( 'NONE', #5525, #2631, #11841, .T. ) ;
#1299=AXIS2_PLACEMENT_3D ( 'NONE', #3317, #5313, #9091 ) ;
#1308=ORIENTED_EDGE ( 'NONE', *, *, #354, .F. ) ;
#1311=DIRECTION ( 'NONE',  ( 0.000000000000000000, 0.000000000000000000, 1.000000000000000000 ) ) ;
#1321=COLOUR_RGB ( '', 0.66274510, 0.83137255, 0.94901961) ;
#1324=ORIENTED_EDGE ( 'NONE', *, *, #3762, .F. ) ;
#1328=EDGE_LOOP ( 'NONE', ( #4671, #5895, #9361, #10082, #6793 ) ) ;
#1340=VERTEX_POINT ( 'NONE', #2135 ) ;
#1350=CARTESIAN_POINT ( 'NONE',  ( 2.500000000000000000, 0.000000000000000000, 0.000000000000000000 ) ) ;
#1369=ADVANCED_FACE ( 'NONE', ( #7680 ), #10727, .F. ) ;
#1406=ORIENTED_EDGE ( 'NONE', *, *, #9688, .F. ) ;
#1411=DIRECTION ( 'NONE',  ( 0.000000000000000000, 1.000000000000000000, -1.224646799147353207E-16 ) ) ;
#1412=FACE_OUTER_BOUND ( 'NONE', #3481, .T. ) ;
#1424=ORIENTED_EDGE ( 'NONE', *, *, #5390, .T. ) ;
#1434=CIRCLE ( 'NONE', #8184, 2.041999999999999815 ) ;
#1442=VERTEX_POINT ( 'NONE', #3007 ) ;
#1451=CIRCLE ( 'NONE', #2047, 2.041999999999999815 ) ;
#1474=DIRECTION ( 'NONE',  ( -1.000000000000000000, -0.000000000000000000, -0.000000000000000000 ) ) ;
#1479=AXIS2_PLACEMENT_3D ( 'NONE', #1276, #4080, #6823 ) ;
#1527=FILL_AREA_STYLE ('',( #4321 ) ) ;
#1546=DIRECTION ( 'NONE',  ( 0.000000000000000000, 1.000000000000000000, -1.287488025362403787E-15 ) ) ;
#1562=ORIENTED_EDGE ( 'NONE', *, *, #3432, .T. ) ;
#1565=ORIENTED_EDGE ( 'NONE', *, *, #10964, .F. ) ;
#1567=PLANE ( 'NONE',  #10870 ) ;
#1612=AXIS2_PLACEMENT_3D ( 'NONE', #9562, #7823, #5032 ) ;
#1613=CARTESIAN_POINT ( 'NONE',  ( 0.000000000000000000, 2.357898499370431722, -2.818925648462311528E-15 ) ) ;
#1616=EDGE_LOOP ( 'NONE', ( #272, #10529, #11415, #3957 ) ) ;
#1623=EDGE_CURVE ( 'NONE', #8974, #12030, #6716, .T. ) ;
#1692=SURFACE_STYLE_FILL_AREA ( #7487 ) ;
#1694=DIRECTION ( 'NONE',  ( 0.000000000000000000, 0.000000000000000000, 1.000000000000000000 ) ) ;
#1697=CARTESIAN_POINT ( 'NONE',  ( 2.500000000000000000, 1.178949249685212974, -2.042000000000001148 ) ) ;
#1703=VECTOR ( 'NONE', #10156, 1000.000000000000114 ) ;
#1708=CARTESIAN_POINT ( 'NONE',  ( 20.55500000000001748, 0.000000000000000000, 2.500000000000000888 ) ) ;
#1740=DIRECTION ( 'NONE',  ( 1.000000000000000000, 0.000000000000000000, 0.000000000000000000 ) ) ;
#1748=DIRECTION ( 'NONE',  ( 1.000000000000000000, 0.000000000000000000, 0.000000000000000000 ) ) ;
#1757=ORIENTED_EDGE ( 'NONE', *, *, #5843, .F. ) ;
#1768=CARTESIAN_POINT ( 'NONE',  ( 2.500000000000000000, 1.178949249685212974, -2.042000000000001148 ) ) ;
#1773=EDGE_CURVE ( 'NONE', #6428, #10397, #5217, .T. ) ;
#1774=ADVANCED_FACE ( 'NONE', ( #1412 ), #7886, .T. ) ;
#1792=DIRECTION ( 'NONE',  ( 0.000000000000000000, 0.000000000000000000, -1.000000000000000000 ) ) ;
#1804=EDGE_CURVE ( 'NONE', #2631, #5525, #7982, .T. ) ;
#1805=CARTESIAN_POINT ( 'NONE',  ( -31.74999999999995737, 0.000000000000000000, 0.000000000000000000 ) ) ;
#1811=DIRECTION ( 'NONE',  ( -1.000000000000000000, -0.000000000000000000, -0.000000000000000000 ) ) ;
#1820=VECTOR ( 'NONE', #8913, 1000.000000000000000 ) ;
#1852=CARTESIAN_POINT ( 'NONE',  ( 5.200000000000002842, 0.000000000000000000, 0.000000000000000000 ) ) ;
#1853=ORIENTED_EDGE ( 'NONE', *, *, #9348, .T. ) ;
#1912=UNCERTAINTY_MEASURE_WITH_UNIT (LENGTH_MEASURE( 1.000000000000000082E-05 ), #3561, 'distance_accuracy_value', 'NONE');
#1930=DIRECTION ( 'NONE',  ( -1.000000000000000000, -0.000000000000000000, -0.000000000000000000 ) ) ;
#1938=DIRECTION ( 'NONE',  ( -0.5000000000000051070, 1.060575238724903217E-16, -0.8660254037844355990 ) ) ;
#1992=ORIENTED_EDGE ( 'NONE', *, *, #448, .T. ) ;
#2005=AXIS2_PLACEMENT_3D ( 'NONE', #3086, #11696, #6893 ) ;
#2006=EDGE_LOOP ( 'NONE', ( #1565, #9158 ) ) ;
#2047=AXIS2_PLACEMENT_3D ( 'NONE', #976, #1096, #84 ) ;
#2088=CARTESIAN_POINT ( 'NONE',  ( 2.500000000000000000, -1.178949249685218748, -2.041999999999998039 ) ) ;
#2101=ORIENTED_EDGE ( 'NONE', *, *, #3184, .T. ) ;
#2135=CARTESIAN_POINT ( 'NONE',  ( 2.500000000000000000, 1.178949249685217415, 2.041999999999998483 ) ) ;
#2136=LINE ( 'NONE', #3129, #6292 ) ;
#2184=ORIENTED_EDGE ( 'NONE', *, *, #10586, .T. ) ;
#2185=AXIS2_PLACEMENT_3D ( 'NONE', #11626, #6879, #10677 ) ;
#2251=CARTESIAN_POINT ( 'NONE',  ( 2.500000000000000000, 2.357898499370431722, -2.818925648462311528E-15 ) ) ;
#2255=ORIENTED_EDGE ( 'NONE', *, *, #4879, .F. ) ;
#2275=AXIS2_PLACEMENT_3D ( 'NONE', #8359, #2881, #4752 ) ;
#2300=VECTOR ( 'NONE', #10486, 1000.000000000000114 ) ;
#2307=AXIS2_PLACEMENT_3D ( 'NONE', #3679, #1748, #7365 ) ;
#2312=CONICAL_SURFACE ( 'NONE', #12283, 2.041999999999999815, 1.047197551196591858 ) ;
#2332=PRESENTATION_STYLE_ASSIGNMENT (( #5210 ) ) ;
#2347=EDGE_LOOP ( 'NONE', ( #132, #1214 ) ) ;
#2349=EDGE_CURVE ( 'NONE', #6428, #1442, #9552, .T. ) ;
#2384=DIRECTION ( 'NONE',  ( -1.000000000000000000, -0.000000000000000000, -0.000000000000000000 ) ) ;
#2411=FACE_OUTER_BOUND ( 'NONE', #5638, .T. ) ;
#2428=ORIENTED_EDGE ( 'NONE', *, *, #11053, .F. ) ;
#2439=ORIENTED_EDGE ( 'NONE', *, *, #3717, .F. ) ;
#2445=DIRECTION ( 'NONE',  ( 0.000000000000000000, 0.000000000000000000, -1.000000000000000000 ) ) ;
#2459=( NAMED_UNIT ( * ) PLANE_ANGLE_UNIT ( ) SI_UNIT ( $, .RADIAN. ) );
#2474=DIRECTION ( 'NONE',  ( 0.000000000000000000, 0.000000000000000000, 1.000000000000000000 ) ) ;
#2482=ORIENTED_EDGE ( 'NONE', *, *, #4520, .T. ) ;
#2490=VECTOR ( 'NONE', #7158, 1000.000000000000114 ) ;
#2502=PLANE ( 'NONE',  #2307 ) ;
#2507=PLANE ( 'NONE',  #11583 ) ;
#2520=LINE ( 'NONE', #11999, #10828 ) ;
#2563=DIRECTION ( 'NONE',  ( 1.000000000000000000, 0.000000000000000000, 0.000000000000000000 ) ) ;
#2573=ORIENTED_EDGE ( 'NONE', *, *, #9688, .T. ) ;
#2578=CARTESIAN_POINT ( 'NONE',  ( 2.500000000000000000, -1.178949249685214307, 2.042000000000001592 ) ) ;
#2622=EDGE_LOOP ( 'NONE', ( #6746, #7064, #6069, #9209 ) ) ;
#2631=VERTEX_POINT ( 'NONE', #6868 ) ;
#2663=AXIS2_PLACEMENT_3D ( 'NONE', #442, #5251, #3193 ) ;
#2679=DIRECTION ( 'NONE',  ( 0.000000000000000000, 0.4999999999999992784, -0.8660254037844389297 ) ) ;
#2680=EDGE_LOOP ( 'NONE', ( #2482, #1202, #8792, #10721, #2255, #1406 ) ) ;
#2685=CARTESIAN_POINT ( 'NONE',  ( 2.500000000000000000, -1.178949249685214307, 2.042000000000001592 ) ) ;
#2702=AXIS2_PLACEMENT_3D ( 'NONE', #974, #4763, #10183 ) ;
#2730=CARTESIAN_POINT ( 'NONE',  ( 0.2500000000000002220, 0.000000000000000000, 0.000000000000000000 ) ) ;
#2761=DIRECTION ( 'NONE',  ( -1.000000000000000000, -0.000000000000000000, -0.000000000000000000 ) ) ;
#2794=CARTESIAN_POINT ( 'NONE',  ( -31.74999999999995737, 0.000000000000000000, 0.000000000000000000 ) ) ;
#2815=AXIS2_PLACEMENT_3D ( 'NONE', #8319, #6151, #11010 ) ;
#2825=DIRECTION ( 'NONE',  ( -1.000000000000000000, -0.000000000000000000, -0.000000000000000000 ) ) ;
#2857=CIRCLE ( 'NONE', #4069, 0.2500000000000002220 ) ;
#2860=CARTESIAN_POINT ( 'NONE',  ( 2.500000000000000000, 1.178949249685212974, -2.042000000000001148 ) ) ;
#2861=FACE_OUTER_BOUND ( 'NONE', #5513, .T. ) ;
#2864=DIRECTION ( 'NONE',  ( 0.000000000000000000, -0.5000000000000009992, -0.8660254037844380415 ) ) ;
#2868=FACE_BOUND ( 'NONE', #2680, .T. ) ;
#2881=DIRECTION ( 'NONE',  ( -1.000000000000000000, -0.000000000000000000, -0.000000000000000000 ) ) ;
#2925=AXIS2_PLACEMENT_3D ( 'NONE', #6751, #8546, #1146 ) ;
#2934=ORIENTED_EDGE ( 'NONE', *, *, #354, .T. ) ;
#2938=CARTESIAN_POINT ( 'NONE',  ( 2.500000000000000000, 2.357898499370431722, -2.818925648462311528E-15 ) ) ;
#2953=LINE ( 'NONE', #5706, #10753 ) ;
#2979=ORIENTED_EDGE ( 'NONE', *, *, #9192, .F. ) ;
#3007=CARTESIAN_POINT ( 'NONE',  ( 5.200000000000002842, 0.000000000000000000, 2.500000000000000444 ) ) ;
#3009=CONICAL_SURFACE ( 'NONE', #11962, 2.055000000000000160, 0.7853981633974639331 ) ;
#3011=VERTEX_POINT ( 'NONE', #2860 ) ;
#3040=DIRECTION ( 'NONE',  ( 0.000000000000000000, -1.000000000000000000, 1.287488025362403787E-15 ) ) ;
#3075=CARTESIAN_POINT ( 'NONE',  ( 0.000000000000000000, -2.357898499370432166, 3.035766082959412415E-15 ) ) ;
#3086=CARTESIAN_POINT ( 'NONE',  ( 5.200000000000002842, 0.000000000000000000, 0.000000000000000000 ) ) ;
#3099=ADVANCED_FACE ( 'NONE', ( #5736 ), #6791, .T. ) ;
#3129=CARTESIAN_POINT ( 'NONE',  ( 21.00000000000000355, 0.000000000000000000, 2.055000000000000160 ) ) ;
#3163=CARTESIAN_POINT ( 'NONE',  ( 4.999999999999997335, 5.204748896376250699E-16, -4.250000000000000000 ) ) ;
#3172=ORIENTED_EDGE ( 'NONE', *, *, #3344, .F. ) ;
#3184=EDGE_CURVE ( 'NONE', #3370, #3011, #4328, .T. ) ;
#3193=DIRECTION ( 'NONE',  ( 0.000000000000000000, 0.000000000000000000, -1.000000000000000000 ) ) ;
#3200=EDGE_CURVE ( 'NONE', #3448, #9390, #7142, .T. ) ;
#3213=EDGE_CURVE ( 'NONE', #9112, #1030, #9313, .T. ) ;
#3222=DIRECTION ( 'NONE',  ( -0.000000000000000000, 0.8660254037844392627, 0.4999999999999990008 ) ) ;
#3224=CARTESIAN_POINT ( 'NONE',  ( 2.500000000000000000, 2.357898499370431722, -2.818925648462311528E-15 ) ) ;
#3290=VECTOR ( 'NONE', #11008, 1000.000000000000000 ) ;
#3317=CARTESIAN_POINT ( 'NONE',  ( 2.500000000000000000, 2.357898499370431722, -2.818925648462311528E-15 ) ) ;
#3319=DIRECTION ( 'NONE',  ( 0.000000000000000000, 0.8660254037844380415, -0.5000000000000012212 ) ) ;
#3342=DIRECTION ( 'NONE',  ( 0.000000000000000000, 0.000000000000000000, 1.000000000000000000 ) ) ;
#3344=EDGE_CURVE ( 'NONE', #4721, #3517, #5947, .T. ) ;
#3360=ORIENTED_EDGE ( 'NONE', *, *, #7641, .F. ) ;
#3370=VERTEX_POINT ( 'NONE', #10246 ) ;
#3380=LINE ( 'NONE', #7245, #1820 ) ;
#3386=VECTOR ( 'NONE', #3607, 1000.000000000000000 ) ;
#3408=DIRECTION ( 'NONE',  ( 0.000000000000000000, 1.224646799147353207E-16, 1.000000000000000000 ) ) ;
#3410=LINE ( 'NONE', #7208, #3290 ) ;
#3432=EDGE_CURVE ( 'NONE', #1442, #6428, #6343, .T. ) ;
#3434=ADVANCED_FACE ( 'NONE', ( #11265 ), #5712, .F. ) ;
#3441=EDGE_LOOP ( 'NONE', ( #989, #4417, #1324, #6599, #562 ) ) ;
#3448=VERTEX_POINT ( 'NONE', #2088 ) ;
#3453=ORIENTED_EDGE ( 'NONE', *, *, #3200, .T. ) ;
#3474=VECTOR ( 'NONE', #8261, 1000.000000000000114 ) ;
#3481=EDGE_LOOP ( 'NONE', ( #9272, #8524, #11564, #10594, #3453 ) ) ;
#3495=ORIENTED_EDGE ( 'NONE', *, *, #1623, .T. ) ;
#3505=CARTESIAN_POINT ( 'NONE',  ( 21.00000000000000000, 2.055000000000000160, 0.000000000000000000 ) ) ;
#3517=VERTEX_POINT ( 'NONE', #6889 ) ;
#3561=( LENGTH_UNIT ( ) NAMED_UNIT ( * ) SI_UNIT ( .MILLI., .METRE. ) );
#3578=DIRECTION ( 'NONE',  ( 0.000000000000000000, 0.000000000000000000, 1.000000000000000000 ) ) ;
#3585=CARTESIAN_POINT ( 'NONE',  ( 0.2500000000000002220, 4.898587196589412829E-16, -4.000000000000000000 ) ) ;
#3600=DIRECTION ( 'NONE',  ( 0.000000000000000000, -0.5000000000000009992, -0.8660254037844380415 ) ) ;
#3607=DIRECTION ( 'NONE',  ( -1.000000000000000000, -0.000000000000000000, -0.000000000000000000 ) ) ;
#3612=VECTOR ( 'NONE', #11722, 1000.000000000000000 ) ;
#3614=AXIS2_PLACEMENT_3D ( 'NONE', #345, #8069, #409 ) ;
#3621=AXIS2_PLACEMENT_3D ( 'NONE', #8657, #7668, #10531 ) ;
#3625=FACE_OUTER_BOUND ( 'NONE', #10039, .T. ) ;
#3632=DIRECTION ( 'NONE',  ( -1.000000000000000000, -0.000000000000000000, -0.000000000000000000 ) ) ;
#3639=AXIS2_PLACEMENT_3D ( 'NONE', #11881, #10686, #7876 ) ;
#3653=FACE_OUTER_BOUND ( 'NONE', #10442, .T. ) ;
#3679=CARTESIAN_POINT ( 'NONE',  ( 2.500000000000000000, 2.357898499370431722, -2.818925648462311528E-15 ) ) ;
#3700=ORIENTED_EDGE ( 'NONE', *, *, #1773, .T. ) ;
#3717=EDGE_CURVE ( 'NONE', #6916, #5925, #5452, .T. ) ;
#3722=PLANE ( 'NONE',  #7832 ) ;
#3762=EDGE_CURVE ( 'NONE', #12030, #1340, #3944, .T. ) ;
#3767=CARTESIAN_POINT ( 'NONE',  ( 2.500000000000000000, 0.000000000000000000, 0.000000000000000000 ) ) ;
#3768=VERTEX_POINT ( 'NONE', #11620 ) ;
#3788=CIRCLE ( 'NONE', #5594, 2.500000000000000888 ) ;
#3802=CARTESIAN_POINT ( 'NONE',  ( 2.500000000000000000, -1.178949249685214307, 2.042000000000001592 ) ) ;
#3805=EDGE_CURVE ( 'NONE', #9112, #1236, #2136, .T. ) ;
#3820=LINE ( 'NONE', #9413, #12037 ) ;
#3826=APPLICATION_CONTEXT ( 'automotive_design' ) ;
#3862=DIRECTION ( 'NONE',  ( 0.000000000000000000, 0.000000000000000000, 1.000000000000000000 ) ) ;
#3943=DIRECTION ( 'NONE',  ( 0.000000000000000000, -1.000000000000000000, 1.287488025362403787E-15 ) ) ;
#3944=LINE ( 'NONE', #66, #11273 ) ;
#3946=ORIENTED_EDGE ( 'NONE', *, *, #3184, .F. ) ;
#3957=ORIENTED_EDGE ( 'NONE', *, *, #4978, .F. ) ;
#3983=ADVANCED_FACE ( 'NONE', ( #4672 ), #2502, .F. ) ;
#3984=DIRECTION ( 'NONE',  ( -1.000000000000000000, -0.000000000000000000, -0.000000000000000000 ) ) ;
#4002=ORIENTED_EDGE ( 'NONE', *, *, #3213, .F. ) ;
#4018=DIRECTION ( 'NONE',  ( -1.000000000000000000, -0.000000000000000000, -0.000000000000000000 ) ) ;
#4025=ADVANCED_FACE ( 'NONE', ( #4550 ), #1567, .T. ) ;
#4049=CARTESIAN_POINT ( 'NONE',  ( 21.00000000000000355, 0.000000000000000000, 0.000000000000000000 ) ) ;
#4065=VERTEX_POINT ( 'NONE', #9462 ) ;
#4069=AXIS2_PLACEMENT_3D ( 'NONE', #3585, #5277, #5400 ) ;
#4074=EDGE_LOOP ( 'NONE', ( #11181, #2184, #4452, #11858, #1078 ) ) ;
#4080=DIRECTION ( 'NONE',  ( -1.000000000000000000, -0.000000000000000000, -0.000000000000000000 ) ) ;
#4093=CLOSED_SHELL ( 'NONE', ( #8608, #5884, #8379, #6886, #5244, #11748, #9530, #3099, #7111, #5011, #10173, #9366, #12157, #12080, #4025, #1369, #10673, #1774, #8962, #10457, #7797, #5037, #5063, #3983, #3434, #5067, #7390 ) ) ;
#4102=CARTESIAN_POINT ( 'NONE',  ( 20.55500000000001748, 0.000000000000000000, 0.000000000000000000 ) ) ;
#4127=CARTESIAN_POINT ( 'NONE',  ( -31.74999999999995737, 0.000000000000000000, 0.000000000000000000 ) ) ;
#4176=EDGE_CURVE ( 'NONE', #10404, #9390, #7843, .T. ) ;
#4217=CARTESIAN_POINT ( 'NONE',  ( 2.500000000000000000, -2.357898499370432166, 3.035766082959412415E-15 ) ) ;
#4274=CARTESIAN_POINT ( 'NONE',  ( 2.500000000000000000, -1.178949249685218748, -2.041999999999998039 ) ) ;
#4294=DIRECTION ( 'NONE',  ( 0.000000000000000000, 0.000000000000000000, 1.000000000000000000 ) ) ;
#4321=FILL_AREA_STYLE_COLOUR ( '', #1321 ) ;
#4325=VERTEX_POINT ( 'NONE', #11214 ) ;
#4328=LINE ( 'NONE', #9116, #8318 ) ;
#4342=AXIS2_PLACEMENT_3D ( 'NONE', #3767, #7512, #11322 ) ;
#4355=ORIENTED_EDGE ( 'NONE', *, *, #11919, .T. ) ;
#4382=AXIS2_PLACEMENT_3D ( 'NONE', #199, #5013, #9793 ) ;
#4388=AXIS2_PLACEMENT_3D ( 'NONE', #9006, #7028, #11959 ) ;
#4406=LINE ( 'NONE', #8445, #9176 ) ;
#4417=ORIENTED_EDGE ( 'NONE', *, *, #10512, .F. ) ;
#4432=DIRECTION ( 'NONE',  ( 0.000000000000000000, 0.5000000000000011102, 0.8660254037844379305 ) ) ;
#4452=ORIENTED_EDGE ( 'NONE', *, *, #7641, .T. ) ;
#4492=CARTESIAN_POINT ( 'NONE',  ( 2.500000000000000000, 2.357898499370431722, -2.818925648462311528E-15 ) ) ;
#4520=EDGE_CURVE ( 'NONE', #7164, #11798, #10637, .T. ) ;
#4535=DIRECTION ( 'NONE',  ( 0.000000000000000000, 0.000000000000000000, -1.000000000000000000 ) ) ;
#4537=EDGE_LOOP ( 'NONE', ( #11933, #1992, #485, #490 ) ) ;
#4541=LINE ( 'NONE', #5613, #8548 ) ;
#4550=FACE_OUTER_BOUND ( 'NONE', #1328, .T. ) ;
#4671=ORIENTED_EDGE ( 'NONE', *, *, #4520, .F. ) ;
#4672=FACE_OUTER_BOUND ( 'NONE', #10726, .T. ) ;
#4701=DIRECTION ( 'NONE',  ( 1.000000000000000000, 0.000000000000000000, 0.000000000000000000 ) ) ;
#4712=CIRCLE ( 'NONE', #2925, 4.250000000000000000 ) ;
#4721=VERTEX_POINT ( 'NONE', #9756 ) ;
#4732=LINE ( 'NONE', #3802, #4905 ) ;
#4749=COLOUR_RGB ( '', 0.66274510, 0.83137255, 0.94901961) ;
#4752=DIRECTION ( 'NONE',  ( 0.000000000000000000, 0.000000000000000000, 1.000000000000000000 ) ) ;
#4761=ORIENTED_EDGE ( 'NONE', *, *, #1240, .T. ) ;
#4763=DIRECTION ( 'NONE',  ( 1.000000000000000000, 0.000000000000000000, 0.000000000000000000 ) ) ;
#4774=CIRCLE ( 'NONE', #2185, 2.055000000000000160 ) ;
#4780=DIRECTION ( 'NONE',  ( 0.000000000000000000, 1.000000000000000000, -1.287488025362403787E-15 ) ) ;
#4812=AXIS2_PLACEMENT_3D ( 'NONE', #8133, #10189, #2474 ) ;
#4853=CARTESIAN_POINT ( 'NONE',  ( 2.500000000000000000, 2.357898499370431722, -2.818925648462311528E-15 ) ) ;
#4879=EDGE_CURVE ( 'NONE', #7492, #9390, #3410, .T. ) ;
#4891=VECTOR ( 'NONE', #10730, 1000.000000000000000 ) ;
#4905=VECTOR ( 'NONE', #2864, 1000.000000000000114 ) ;
#4959=ORIENTED_EDGE ( 'NONE', *, *, #3344, .T. ) ;
#4977=FACE_OUTER_BOUND ( 'NONE', #5687, .T. ) ;
#4978=EDGE_CURVE ( 'NONE', #1236, #1442, #193, .T. ) ;
#5011=ADVANCED_FACE ( 'NONE', ( #259 ), #5075, .T. ) ;
#5013=DIRECTION ( 'NONE',  ( -1.000000000000000000, -0.000000000000000000, -0.000000000000000000 ) ) ;
#5032=DIRECTION ( 'NONE',  ( 1.000000000000000000, 0.000000000000000000, 0.000000000000000000 ) ) ;
#5037=ADVANCED_FACE ( 'NONE', ( #8971 ), #10791, .F. ) ;
#5050=CONICAL_SURFACE ( 'NONE', #5453, 2.041999999999999815, 1.047197551196591858 ) ;
#5063=ADVANCED_FACE ( 'NONE', ( #10036 ), #7977, .F. ) ;
#5067=ADVANCED_FACE ( 'NONE', ( #568 ), #6993, .F. ) ;
#5073=VECTOR ( 'NONE', #959, 1000.000000000000114 ) ;
#5075=CYLINDRICAL_SURFACE ( 'NONE', #5461, 2.500000000000000444 ) ;
#5159=DIRECTION ( 'NONE',  ( 0.000000000000000000, 0.000000000000000000, 1.000000000000000000 ) ) ;
#5163=CARTESIAN_POINT ( 'NONE',  ( 2.500000000000000000, -2.357898499370432166, 3.035766082959412415E-15 ) ) ;
#5171=EDGE_LOOP ( 'NONE', ( #402, #6295, #6300, #2979 ) ) ;
#5210=SURFACE_STYLE_USAGE ( .BOTH. , #10809 ) ;
#5217=CIRCLE ( 'NONE', #3614, 0.2000000000000000944 ) ;
#5229=LINE ( 'NONE', #11903, #10954 ) ;
#5244=ADVANCED_FACE ( 'NONE', ( #11300 ), #10406, .T. ) ;
#5251=DIRECTION ( 'NONE',  ( 1.000000000000000000, 0.000000000000000000, 0.000000000000000000 ) ) ;
#5271=( NAMED_UNIT ( * ) SI_UNIT ( $, .STERADIAN. ) SOLID_ANGLE_UNIT ( ) );
#5277=DIRECTION ( 'NONE',  ( -0.000000000000000000, 1.000000000000000000, 1.224646799147353207E-16 ) ) ;
#5313=DIRECTION ( 'NONE',  ( 1.000000000000000000, 0.000000000000000000, 0.000000000000000000 ) ) ;
#5321=EDGE_CURVE ( 'NONE', #3517, #3448, #6612, .T. ) ;
#5366=CIRCLE ( 'NONE', #9934, 4.250000000000000000 ) ;
#5390=EDGE_CURVE ( 'NONE', #8667, #4721, #7666, .T. ) ;
#5400=DIRECTION ( 'NONE',  ( 0.000000000000000000, -1.224646799147353454E-16, 1.000000000000000000 ) ) ;
#5401=DIRECTION ( 'NONE',  ( -1.000000000000000000, -0.000000000000000000, -0.000000000000000000 ) ) ;
#5452=LINE ( 'NONE', #8482, #2300 ) ;
#5453=AXIS2_PLACEMENT_3D ( 'NONE', #1350, #1474, #5159 ) ;
#5461=AXIS2_PLACEMENT_3D ( 'NONE', #4127, #10312, #5762 ) ;
#5467=DIRECTION ( 'NONE',  ( -1.000000000000000000, -0.000000000000000000, -0.000000000000000000 ) ) ;
#5472=TOROIDAL_SURFACE ( 'NONE', #12246, 4.000000000000000000, 0.2500000000000000000 ) ;
#5513=EDGE_LOOP ( 'NONE', ( #8301, #4761, #1164, #279 ) ) ;
#5521=DIRECTION ( 'NONE',  ( 0.000000000000000000, 1.000000000000000000, -1.287488025362403787E-15 ) ) ;
#5525=VERTEX_POINT ( 'NONE', #11970 ) ;
#5549=DIRECTION ( 'NONE',  ( 0.000000000000000000, 0.000000000000000000, 1.000000000000000000 ) ) ;
#5551=CYLINDRICAL_SURFACE ( 'NONE', #6375, 4.250000000000000000 ) ;
#5586=CARTESIAN_POINT ( 'NONE',  ( 5.000000000000002665, 3.306546357697854226E-16, 2.700000000000000622 ) ) ;
#5594=AXIS2_PLACEMENT_3D ( 'NONE', #4102, #6911, #9512 ) ;
#5613=CARTESIAN_POINT ( 'NONE',  ( 2.500000000000000000, 2.357898499370431722, -2.818925648462311528E-15 ) ) ;
#5622=EDGE_LOOP ( 'NONE', ( #9090, #7420 ) ) ;
#5623=SHAPE_REPRESENTATION_RELATIONSHIP ( 'NONE' , 'NONE' ,  #778, #6020 ) ;
#5636=CARTESIAN_POINT ( 'NONE',  ( 21.00000000000000355, 2.516649172247811061E-16, -2.055000000000000160 ) ) ;
#5638=EDGE_LOOP ( 'NONE', ( #11553, #6240, #3700, #10074 ) ) ;
#5681=( NAMED_UNIT ( * ) PLANE_ANGLE_UNIT ( ) SI_UNIT ( $, .RADIAN. ) );
#5686=DIRECTION ( 'NONE',  ( 0.000000000000000000, 0.8660254037844380415, -0.5000000000000009992 ) ) ;
#5687=EDGE_LOOP ( 'NONE', ( #12196, #8467, #7219, #554 ) ) ;
#5706=CARTESIAN_POINT ( 'NONE',  ( 2.500000000000000000, 1.178949249685212974, -2.042000000000001148 ) ) ;
#5712=PLANE ( 'NONE',  #2702 ) ;
#5736=FACE_OUTER_BOUND ( 'NONE', #2622, .T. ) ;
#5737=CARTESIAN_POINT ( 'NONE',  ( 0.000000000000000000, -1.178949249685214307, 2.042000000000001592 ) ) ;
#5762=DIRECTION ( 'NONE',  ( 0.000000000000000000, 0.000000000000000000, 1.000000000000000000 ) ) ;
#5843=EDGE_CURVE ( 'NONE', #4721, #3448, #11527, .T. ) ;
#5854=CARTESIAN_POINT ( 'NONE',  ( 2.500000000000000000, 2.629050547790028946E-15, 2.042000000000000259 ) ) ;
#5855=VECTOR ( 'NONE', #4018, 1000.000000000000000 ) ;
#5884=ADVANCED_FACE ( 'NONE', ( #4977 ), #5472, .T. ) ;
#5895=ORIENTED_EDGE ( 'NONE', *, *, #11817, .F. ) ;
#5903=ORIENTED_EDGE ( 'NONE', *, *, #9348, .F. ) ;
#5906=VECTOR ( 'NONE', #7023, 1000.000000000000000 ) ;
#5911=ORIENTED_EDGE ( 'NONE', *, *, #6349, .T. ) ;
#5925=VERTEX_POINT ( 'NONE', #5163 ) ;
#5947=CIRCLE ( 'NONE', #4342, 2.041999999999999815 ) ;
#6018=FACE_OUTER_BOUND ( 'NONE', #11711, .T. ) ;
#6020=ADVANCED_BREP_SHAPE_REPRESENTATION ( '', ( #8859, #1612 ), #6744 ) ;
#6041=EDGE_CURVE ( 'NONE', #5925, #3517, #11080, .T. ) ;
#6069=ORIENTED_EDGE ( 'NONE', *, *, #9192, .T. ) ;
#6122=DIRECTION ( 'NONE',  ( 0.000000000000000000, 0.000000000000000000, -1.000000000000000000 ) ) ;
#6151=DIRECTION ( 'NONE',  ( -1.000000000000000000, -0.000000000000000000, -0.000000000000000000 ) ) ;
#6181=DIRECTION ( 'NONE',  ( 1.000000000000000000, 0.000000000000000000, 0.000000000000000000 ) ) ;
#6221=CARTESIAN_POINT ( 'NONE',  ( 5.200000000000002842, 0.000000000000000000, 0.000000000000000000 ) ) ;
#6233=CARTESIAN_POINT ( 'NONE',  ( 4.999999999999997335, 0.000000000000000000, 0.000000000000000000 ) ) ;
#6240=ORIENTED_EDGE ( 'NONE', *, *, #2349, .F. ) ;
#6292=VECTOR ( 'NONE', #1143, 1000.000000000000114 ) ;
#6294=CARTESIAN_POINT ( 'NONE',  ( 2.500000000000000000, -2.357898499370432166, 3.035766082959412415E-15 ) ) ;
#6295=ORIENTED_EDGE ( 'NONE', *, *, #1138, .T. ) ;
#6300=ORIENTED_EDGE ( 'NONE', *, *, #11024, .T. ) ;
#6329=ORIENTED_EDGE ( 'NONE', *, *, #8074, .F. ) ;
#6343=CIRCLE ( 'NONE', #10058, 2.500000000000000444 ) ;
#6349=EDGE_CURVE ( 'NONE', #3517, #6916, #9440, .T. ) ;
#6370=DIRECTION ( 'NONE',  ( 0.000000000000000000, 0.000000000000000000, -1.000000000000000000 ) ) ;
#6375=AXIS2_PLACEMENT_3D ( 'NONE', #2794, #11156, #11221 ) ;
#6428=VERTEX_POINT ( 'NONE', #8666 ) ;
#6442=CARTESIAN_POINT ( 'NONE',  ( 2.500000000000000000, 0.000000000000000000, 0.000000000000000000 ) ) ;
#6511=EDGE_LOOP ( 'NONE', ( #2573, #5903, #3946, #9083, #10917 ) ) ;
#6590=VECTOR ( 'NONE', #444, 1000.000000000000114 ) ;
#6596=DIRECTION ( 'NONE',  ( -1.000000000000000000, -0.000000000000000000, -0.000000000000000000 ) ) ;
#6599=ORIENTED_EDGE ( 'NONE', *, *, #1623, .F. ) ;
#6612=LINE ( 'NONE', #9466, #1703 ) ;
#6687=ORIENTED_EDGE ( 'NONE', *, *, #8578, .F. ) ;
#6716=LINE ( 'NONE', #11164, #12181 ) ;
#6720=DIRECTION ( 'NONE',  ( 0.000000000000000000, 0.000000000000000000, 1.000000000000000000 ) ) ;
#6744=( GEOMETRIC_REPRESENTATION_CONTEXT ( 3 ) GLOBAL_UNCERTAINTY_ASSIGNED_CONTEXT ( ( #30 ) ) GLOBAL_UNIT_ASSIGNED_CONTEXT ( ( #8409, #5681, #762 ) ) REPRESENTATION_CONTEXT ( 'NONE', 'WORKASPACE' ) );
#6746=ORIENTED_EDGE ( 'NONE', *, *, #1138, .F. ) ;
#6751=CARTESIAN_POINT ( 'NONE',  ( 4.999999999999997335, 0.000000000000000000, 0.000000000000000000 ) ) ;
#6791=CYLINDRICAL_SURFACE ( 'NONE', #10704, 4.250000000000000000 ) ;
#6793=ORIENTED_EDGE ( 'NONE', *, *, #10512, .T. ) ;
#6823=DIRECTION ( 'NONE',  ( 0.000000000000000000, 0.000000000000000000, 1.000000000000000000 ) ) ;
#6845=DIRECTION ( 'NONE',  ( 0.000000000000000000, -0.4999999999999993339, 0.8660254037844390407 ) ) ;
#6850=CIRCLE ( 'NONE', #1479, 2.041999999999999815 ) ;
#6868=CARTESIAN_POINT ( 'NONE',  ( 0.000000000000000000, 5.051668046482832750E-16, -4.000000000000000000 ) ) ;
#6879=DIRECTION ( 'NONE',  ( -1.000000000000000000, -0.000000000000000000, -0.000000000000000000 ) ) ;
#6884=VERTEX_POINT ( 'NONE', #5737 ) ;
#6886=ADVANCED_FACE ( 'NONE', ( #2861 ), #8613, .T. ) ;
#6887=CARTESIAN_POINT ( 'NONE',  ( 21.00000000000000355, 2.789133085058097101E-16, -2.055000000000000160 ) ) ;
#6889=CARTESIAN_POINT ( 'NONE',  ( 2.500000000000000000, -1.768423874527825568, -1.020999999999998575 ) ) ;
#6893=DIRECTION ( 'NONE',  ( 0.000000000000000000, 0.000000000000000000, -1.000000000000000000 ) ) ;
#6904=DIRECTION ( 'NONE',  ( 0.000000000000000000, -0.4999999999999989453, 0.8660254037844391517 ) ) ;
#6911=DIRECTION ( 'NONE',  ( -1.000000000000000000, -0.000000000000000000, -0.000000000000000000 ) ) ;
#6916=VERTEX_POINT ( 'NONE', #11715 ) ;
#6967=DIRECTION ( 'NONE',  ( 0.000000000000000000, 0.000000000000000000, -1.000000000000000000 ) ) ;
#6993=PLANE ( 'NONE',  #10849 ) ;
#6995=CARTESIAN_POINT ( 'NONE',  ( 5.000000000000002665, 0.000000000000000000, -2.700000000000000622 ) ) ;
#7022=DIRECTION ( 'NONE',  ( -1.000000000000000000, -0.000000000000000000, -0.000000000000000000 ) ) ;
#7023=DIRECTION ( 'NONE',  ( 0.000000000000000000, -0.4999999999999993339, 0.8660254037844390407 ) ) ;
#7028=DIRECTION ( 'NONE',  ( -1.000000000000000000, -0.000000000000000000, -0.000000000000000000 ) ) ;
#7064=ORIENTED_EDGE ( 'NONE', *, *, #9144, .T. ) ;
#7068=LINE ( 'NONE', #8923, #5855 ) ;
#7111=ADVANCED_FACE ( 'NONE', ( #743, #12151 ), #3722, .T. ) ;
#7138=EDGE_CURVE ( 'NONE', #6884, #10404, #11088, .T. ) ;
#7142=LINE ( 'NONE', #4274, #10911 ) ;
#7158=DIRECTION ( 'NONE',  ( 0.000000000000000000, 0.4999999999999990008, -0.8660254037844391517 ) ) ;
#7164=VERTEX_POINT ( 'NONE', #1613 ) ;
#7208=CARTESIAN_POINT ( 'NONE',  ( 0.000000000000000000, 1.178949249685212974, -2.042000000000001148 ) ) ;
#7219=ORIENTED_EDGE ( 'NONE', *, *, #1282, .F. ) ;
#7231=FACE_OUTER_BOUND ( 'NONE', #5171, .T. ) ;
#7245=CARTESIAN_POINT ( 'NONE',  ( 2.500000000000000000, 1.178949249685217415, 2.041999999999998483 ) ) ;
#7278=CARTESIAN_POINT ( 'NONE',  ( 2.500000000000000000, -2.357898499370432166, 3.035766082959412415E-15 ) ) ;
#7296=( GEOMETRIC_REPRESENTATION_CONTEXT ( 3 ) GLOBAL_UNCERTAINTY_ASSIGNED_CONTEXT ( ( #11003 ) ) GLOBAL_UNIT_ASSIGNED_CONTEXT ( ( #7995, #2459, #5271 ) ) REPRESENTATION_CONTEXT ( 'NONE', 'WORKASPACE' ) );
#7320=ORIENTED_EDGE ( 'NONE', *, *, #7340, .T. ) ;
#7340=EDGE_CURVE ( 'NONE', #1442, #875, #9207, .T. ) ;
#7353=LINE ( 'NONE', #12218, #3386 ) ;
#7356=ORIENTED_EDGE ( 'NONE', *, *, #448, .F. ) ;
#7365=DIRECTION ( 'NONE',  ( 0.000000000000000000, 0.000000000000000000, -1.000000000000000000 ) ) ;
#7367=SURFACE_SIDE_STYLE ('',( #1692 ) ) ;
#7390=ADVANCED_FACE ( 'NONE', ( #9937 ), #5050, .F. ) ;
#7391=ORIENTED_EDGE ( 'NONE', *, *, #4978, .T. ) ;
#7420=ORIENTED_EDGE ( 'NONE', *, *, #10536, .T. ) ;
#7487=FILL_AREA_STYLE ('',( #822 ) ) ;
#7492=VERTEX_POINT ( 'NONE', #8881 ) ;
#7497=MECHANICAL_DESIGN_GEOMETRIC_PRESENTATION_REPRESENTATION('',(#11886),#7296);
#7505=DIRECTION ( 'NONE',  ( 0.000000000000000000, -1.287488025362403787E-15, -1.000000000000000000 ) ) ;
#7512=DIRECTION ( 'NONE',  ( -1.000000000000000000, -0.000000000000000000, -0.000000000000000000 ) ) ;
#7590=CARTESIAN_POINT ( 'NONE',  ( 2.500000000000000000, 1.178949249685212974, -2.042000000000001148 ) ) ;
#7641=EDGE_CURVE ( 'NONE', #12030, #11226, #1451, .T. ) ;
#7661=ORIENTED_EDGE ( 'NONE', *, *, #10586, .F. ) ;
#7666=LINE ( 'NONE', #7790, #9220 ) ;
#7668=DIRECTION ( 'NONE',  ( -1.000000000000000000, 0.000000000000000000, -0.000000000000000000 ) ) ;
#7680=FACE_OUTER_BOUND ( 'NONE', #3441, .T. ) ;
#7790=CARTESIAN_POINT ( 'NONE',  ( 2.500000000000000000, 2.500728763858895382E-16, -2.041999999999999815 ) ) ;
#7797=ADVANCED_FACE ( 'NONE', ( #6018 ), #8055, .F. ) ;
#7823=DIRECTION ( 'NONE',  ( 0.000000000000000000, 0.000000000000000000, 1.000000000000000000 ) ) ;
#7832=AXIS2_PLACEMENT_3D ( 'NONE', #9444, #11280, #4535 ) ;
#7843=LINE ( 'NONE', #10712, #2490 ) ;
#7858=CARTESIAN_POINT ( 'NONE',  ( 2.500000000000000000, -1.178949249685214307, 2.042000000000001592 ) ) ;
#7876=DIRECTION ( 'NONE',  ( 0.000000000000000000, 0.000000000000000000, -1.000000000000000000 ) ) ;
#7886=PLANE ( 'NONE',  #11593 ) ;
#7894=VECTOR ( 'NONE', #2825, 1000.000000000000000 ) ;
#7960=ORIENTED_EDGE ( 'NONE', *, *, #11113, .F. ) ;
#7962=CARTESIAN_POINT ( 'NONE',  ( 0.2500000000000002220, 0.000000000000000000, 0.000000000000000000 ) ) ;
#7977=PLANE ( 'NONE',  #1299 ) ;
#7982=CIRCLE ( 'NONE', #8784, 4.000000000000000000 ) ;
#7995=( LENGTH_UNIT ( ) NAMED_UNIT ( * ) SI_UNIT ( .MILLI., .METRE. ) );
#8025=DIRECTION ( 'NONE',  ( -1.000000000000000000, -0.000000000000000000, -0.000000000000000000 ) ) ;
#8055=PLANE ( 'NONE',  #3639 ) ;
#8069=DIRECTION ( 'NONE',  ( 0.000000000000000000, -1.000000000000000000, 0.000000000000000000 ) ) ;
#8074=EDGE_CURVE ( 'NONE', #8974, #6916, #4732, .T. ) ;
#8092=ORIENTED_EDGE ( 'NONE', *, *, #11424, .F. ) ;
#8102=CARTESIAN_POINT ( 'NONE',  ( 2.500000000000000000, 2.357898499370431722, -2.818925648462311528E-15 ) ) ;
#8121=ORIENTED_EDGE ( 'NONE', *, *, #7138, .F. ) ;
#8133=CARTESIAN_POINT ( 'NONE',  ( 20.55500000000001748, 0.000000000000000000, 0.000000000000000000 ) ) ;
#8184=AXIS2_PLACEMENT_3D ( 'NONE', #825, #10219, #12112 ) ;
#8223=SURFACE_STYLE_USAGE ( .BOTH. , #7367 ) ;
#8225=CARTESIAN_POINT ( 'NONE',  ( 0.000000000000000000, -1.178949249685218748, -2.041999999999998039 ) ) ;
#8228=AXIS2_PLACEMENT_3D ( 'NONE', #11168, #1811, #1694 ) ;
#8261=DIRECTION ( 'NONE',  ( 0.000000000000000000, 0.4999999999999990008, -0.8660254037844391517 ) ) ;
#8295=AXIS2_PLACEMENT_3D ( 'NONE', #3505, #2563, #6370 ) ;
#8301=ORIENTED_EDGE ( 'NONE', *, *, #3213, .T. ) ;
#8318=VECTOR ( 'NONE', #236, 999.9999999999997726 ) ;
#8319=CARTESIAN_POINT ( 'NONE',  ( 2.500000000000000000, 0.000000000000000000, 0.000000000000000000 ) ) ;
#8328=CARTESIAN_POINT ( 'NONE',  ( 0.000000000000000000, -1.178949249685214307, 2.042000000000001592 ) ) ;
#8334=ORIENTED_EDGE ( 'NONE', *, *, #3432, .F. ) ;
#8338=AXIS2_PLACEMENT_3D ( 'NONE', #2730, #1740, #5549 ) ;
#8344=DIRECTION ( 'NONE',  ( 0.000000000000000000, -0.8660254037844390407, -0.4999999999999993339 ) ) ;
#8359=CARTESIAN_POINT ( 'NONE',  ( 0.000000000000000000, 0.000000000000000000, 0.000000000000000000 ) ) ;
#8379=ADVANCED_FACE ( 'NONE', ( #10390 ), #10261, .F. ) ;
#8409=( LENGTH_UNIT ( ) NAMED_UNIT ( * ) SI_UNIT ( .MILLI., .METRE. ) );
#8431=ORIENTED_EDGE ( 'NONE', *, *, #8074, .T. ) ;
#8445=CARTESIAN_POINT ( 'NONE',  ( 0.000000000000000000, 2.357898499370431722, -2.818925648462311528E-15 ) ) ;
#8467=ORIENTED_EDGE ( 'NONE', *, *, #639, .T. ) ;
#8479=DIRECTION ( 'NONE',  ( 0.000000000000000000, 0.000000000000000000, 1.000000000000000000 ) ) ;
#8482=CARTESIAN_POINT ( 'NONE',  ( 2.500000000000000000, -1.178949249685214307, 2.042000000000001592 ) ) ;
#8500=CARTESIAN_POINT ( 'NONE',  ( 2.500000000000000000, 0.000000000000000000, 0.000000000000000000 ) ) ;
#8524=ORIENTED_EDGE ( 'NONE', *, *, #10893, .F. ) ;
#8544=EDGE_CURVE ( 'NONE', #4065, #5525, #936, .T. ) ;
#8546=DIRECTION ( 'NONE',  ( -1.000000000000000000, -0.000000000000000000, -0.000000000000000000 ) ) ;
#8548=VECTOR ( 'NONE', #812, 1000.000000000000000 ) ;
#8557=PRODUCT_DEFINITION_SHAPE ( 'NONE', 'NONE',  #11612 ) ;
#8578=EDGE_CURVE ( 'NONE', #11226, #1340, #11953, .T. ) ;
#8605=DIRECTION ( 'NONE',  ( 0.000000000000000000, -0.5000000000000013323, -0.8660254037844380415 ) ) ;
#8608=ADVANCED_FACE ( 'NONE', ( #3653 ), #2312, .F. ) ;
#8613=CONICAL_SURFACE ( 'NONE', #9608, 2.055000000000000160, 0.7853981633974639331 ) ;
#8637=ORIENTED_EDGE ( 'NONE', *, *, #9434, .F. ) ;
#8647=CARTESIAN_POINT ( 'NONE',  ( 21.00000000000000355, 0.000000000000000000, 0.000000000000000000 ) ) ;
#8657=CARTESIAN_POINT ( 'NONE',  ( 0.000000000000000000, 0.000000000000000000, 0.000000000000000000 ) ) ;
#8666=CARTESIAN_POINT ( 'NONE',  ( 5.200000000000002842, 3.061616997868383634E-16, -2.500000000000000444 ) ) ;
#8667=VERTEX_POINT ( 'NONE', #664 ) ;
#8674=APPLICATION_CONTEXT ( 'automotive_design' ) ;
#8681=AXIS2_PLACEMENT_3D ( 'NONE', #11898, #10762, #10007 ) ;
#8692=EDGE_LOOP ( 'NONE', ( #2101, #2934, #12159 ) ) ;
#8731=CARTESIAN_POINT ( 'NONE',  ( -31.74999999999995737, 0.000000000000000000, 2.500000000000000444 ) ) ;
#8732=LINE ( 'NONE', #10488, #7894 ) ;
#8767=CIRCLE ( 'NONE', #11974, 2.700000000000000622 ) ;
#8784=AXIS2_PLACEMENT_3D ( 'NONE', #10696, #7022, #10817 ) ;
#8792=ORIENTED_EDGE ( 'NONE', *, *, #7138, .T. ) ;
#8809=SURFACE_STYLE_FILL_AREA ( #1527 ) ;
#8812=VECTOR ( 'NONE', #3600, 1000.000000000000114 ) ;
#8859=MANIFOLD_SOLID_BREP ( 'Hex', #4093 ) ;
#8881=CARTESIAN_POINT ( 'NONE',  ( 0.000000000000000000, 1.178949249685212974, -2.042000000000001148 ) ) ;
#8887=EDGE_LOOP ( 'NONE', ( #11368, #4355, #7391, #1562 ) ) ;
#8889=VECTOR ( 'NONE', #10285, 1000.000000000000000 ) ;
#8913=DIRECTION ( 'NONE',  ( -1.000000000000000000, -0.000000000000000000, -0.000000000000000000 ) ) ;
#8921=VERTEX_POINT ( 'NONE', #11883 ) ;
#8923=CARTESIAN_POINT ( 'NONE',  ( -31.74999999999995737, 3.061616997868383634E-16, -2.500000000000000444 ) ) ;
#8962=ADVANCED_FACE ( 'NONE', ( #10363 ), #9107, .F. ) ;
#8971=FACE_OUTER_BOUND ( 'NONE', #11001, .T. ) ;
#8974=VERTEX_POINT ( 'NONE', #2578 ) ;
#9006=CARTESIAN_POINT ( 'NONE',  ( 0.2500000000000002220, 0.000000000000000000, 0.000000000000000000 ) ) ;
#9009=AXIS2_PLACEMENT_3D ( 'NONE', #10758, #1411, #3408 ) ;
#9031=VECTOR ( 'NONE', #3040, 1000.000000000000000 ) ;
#9062=AXIS2_PLACEMENT_3D ( 'NONE', #1852, #10265, #1792 ) ;
#9083=ORIENTED_EDGE ( 'NONE', *, *, #1222, .F. ) ;
#9090=ORIENTED_EDGE ( 'NONE', *, *, #11424, .T. ) ;
#9091=DIRECTION ( 'NONE',  ( 0.000000000000000000, 0.000000000000000000, -1.000000000000000000 ) ) ;
#9093=LINE ( 'NONE', #9914, #6590 ) ;
#9107=PLANE ( 'NONE',  #12089 ) ;
#9112=VERTEX_POINT ( 'NONE', #12308 ) ;
#9116=CARTESIAN_POINT ( 'NONE',  ( 2.500000000000000000, 2.357898499370431722, -2.818925648462311528E-15 ) ) ;
#9144=EDGE_CURVE ( 'NONE', #12045, #8921, #4712, .T. ) ;
#9158=ORIENTED_EDGE ( 'NONE', *, *, #9144, .F. ) ;
#9176=VECTOR ( 'NONE', #801, 999.9999999999997726 ) ;
#9192=EDGE_CURVE ( 'NONE', #8921, #4065, #8732, .T. ) ;
#9207=CIRCLE ( 'NONE', #9009, 0.2000000000000000944 ) ;
#9209=ORIENTED_EDGE ( 'NONE', *, *, #11053, .T. ) ;
#9220=VECTOR ( 'NONE', #1938, 1000.000000000000114 ) ;
#9272=ORIENTED_EDGE ( 'NONE', *, *, #4176, .F. ) ;
#9313=CIRCLE ( 'NONE', #158, 2.055000000000000160 ) ;
#9348=EDGE_CURVE ( 'NONE', #3011, #7492, #260, .T. ) ;
#9361=ORIENTED_EDGE ( 'NONE', *, *, #11212, .T. ) ;
#9366=ADVANCED_FACE ( 'NONE', ( #11044 ), #11107, .T. ) ;
#9369=CARTESIAN_POINT ( 'NONE',  ( 5.200000000000002842, 0.000000000000000000, 0.000000000000000000 ) ) ;
#9390=VERTEX_POINT ( 'NONE', #8225 ) ;
#9394=DIRECTION ( 'NONE',  ( 0.000000000000000000, 0.000000000000000000, 1.000000000000000000 ) ) ;
#9401=FACE_OUTER_BOUND ( 'NONE', #2347, .T. ) ;
#9413=CARTESIAN_POINT ( 'NONE',  ( 2.500000000000000000, 2.357898499370431722, -2.818925648462311528E-15 ) ) ;
#9434=EDGE_CURVE ( 'NONE', #11226, #3370, #1434, .T. ) ;
#9440=CIRCLE ( 'NONE', #10244, 2.041999999999999815 ) ;
#9444=CARTESIAN_POINT ( 'NONE',  ( 5.000000000000000888, 4.250000000000000000, 0.000000000000000000 ) ) ;
#9462=CARTESIAN_POINT ( 'NONE',  ( 0.2500000000000002220, 0.000000000000000000, 4.250000000000000000 ) ) ;
#9466=CARTESIAN_POINT ( 'NONE',  ( 2.500000000000000000, -2.357898499370432166, 3.035766082959412415E-15 ) ) ;
#9512=DIRECTION ( 'NONE',  ( 0.000000000000000000, 0.000000000000000000, 1.000000000000000000 ) ) ;
#9523=SHAPE_DEFINITION_REPRESENTATION ( #8557, #778 ) ;
#9530=ADVANCED_FACE ( 'NONE', ( #2868, #9401 ), #10343, .T. ) ;
#9552=CIRCLE ( 'NONE', #2005, 2.500000000000000444 ) ;
#9562=CARTESIAN_POINT ( 'NONE',  ( 0.000000000000000000, 0.000000000000000000, 0.000000000000000000 ) ) ;
#9604=ORIENTED_EDGE ( 'NONE', *, *, #9798, .F. ) ;
#9608=AXIS2_PLACEMENT_3D ( 'NONE', #8647, #1930, #3862 ) ;
#9634=CARTESIAN_POINT ( 'NONE',  ( 0.2500000000000002220, 0.000000000000000000, 0.000000000000000000 ) ) ;
#9688=EDGE_CURVE ( 'NONE', #7164, #7492, #4406, .T. ) ;
#9750=CIRCLE ( 'NONE', #4382, 2.700000000000000622 ) ;
#9756=CARTESIAN_POINT ( 'NONE',  ( 2.500000000000000000, -2.629050547790028551E-15, -2.041999999999999815 ) ) ;
#9766=EDGE_LOOP ( 'NONE', ( #10608, #1218, #1757, #1308, #1853 ) ) ;
#9793=DIRECTION ( 'NONE',  ( 0.000000000000000000, 0.000000000000000000, -1.000000000000000000 ) ) ;
#9798=EDGE_CURVE ( 'NONE', #6916, #12030, #11987, .T. ) ;
#9842=EDGE_CURVE ( 'NONE', #1236, #3768, #10178, .T. ) ;
#9847=DIRECTION ( 'NONE',  ( -0.000000000000000000, 1.287488025362403787E-15, 1.000000000000000000 ) ) ;
#9852=DIRECTION ( 'NONE',  ( -1.000000000000000000, -0.000000000000000000, -0.000000000000000000 ) ) ;
#9914=CARTESIAN_POINT ( 'NONE',  ( 2.500000000000000000, 0.000000000000000000, 2.041999999999999815 ) ) ;
#9934=AXIS2_PLACEMENT_3D ( 'NONE', #7962, #553, #1311 ) ;
#9937=FACE_OUTER_BOUND ( 'NONE', #4074, .T. ) ;
#9972=CIRCLE ( 'NONE', #185, 4.250000000000000000 ) ;
#10007=DIRECTION ( 'NONE',  ( 0.000000000000000000, 0.000000000000000000, -1.000000000000000000 ) ) ;
#10036=FACE_OUTER_BOUND ( 'NONE', #11673, .T. ) ;
#10039=EDGE_LOOP ( 'NONE', ( #8121, #7960, #8431, #12211, #10500 ) ) ;
#10058=AXIS2_PLACEMENT_3D ( 'NONE', #9369, #4701, #10436 ) ;
#10074=ORIENTED_EDGE ( 'NONE', *, *, #10536, .F. ) ;
#10082=ORIENTED_EDGE ( 'NONE', *, *, #8578, .T. ) ;
#10113=STYLED_ITEM ( 'NONE', ( #12232 ), #6020 ) ;
#10130=CIRCLE ( 'NONE', #8338, 4.250000000000000000 ) ;
#10156=DIRECTION ( 'NONE',  ( 0.000000000000000000, 0.4999999999999990008, -0.8660254037844391517 ) ) ;
#10173=ADVANCED_FACE ( 'NONE', ( #11373 ), #3009, .T. ) ;
#10178=CIRCLE ( 'NONE', #4812, 2.500000000000000888 ) ;
#10183=DIRECTION ( 'NONE',  ( 0.000000000000000000, 0.000000000000000000, -1.000000000000000000 ) ) ;
#10189=DIRECTION ( 'NONE',  ( -1.000000000000000000, -0.000000000000000000, -0.000000000000000000 ) ) ;
#10219=DIRECTION ( 'NONE',  ( -1.000000000000000000, -0.000000000000000000, -0.000000000000000000 ) ) ;
#10244=AXIS2_PLACEMENT_3D ( 'NONE', #6442, #3632, #8479 ) ;
#10246=CARTESIAN_POINT ( 'NONE',  ( 2.500000000000000000, 1.768423874527822459, -1.021000000000002794 ) ) ;
#10261=TOROIDAL_SURFACE ( 'NONE', #9062, 2.700000000000000622, 0.2000000000000000111 ) ;
#10265=DIRECTION ( 'NONE',  ( 1.000000000000000000, 0.000000000000000000, 0.000000000000000000 ) ) ;
#10285=DIRECTION ( 'NONE',  ( -1.000000000000000000, -0.000000000000000000, -0.000000000000000000 ) ) ;
#10312=DIRECTION ( 'NONE',  ( -1.000000000000000000, -0.000000000000000000, -0.000000000000000000 ) ) ;
#10319=ORIENTED_EDGE ( 'NONE', *, *, #639, .F. ) ;
#10341=( NAMED_UNIT ( * ) SI_UNIT ( $, .STERADIAN. ) SOLID_ANGLE_UNIT ( ) );
#10343=PLANE ( 'NONE',  #3621 ) ;
#10344=DIRECTION ( 'NONE',  ( 0.000000000000000000, 0.5000000000000009992, 0.8660254037844380415 ) ) ;
#10361=TOROIDAL_SURFACE ( 'NONE', #11766, 2.700000000000000622, 0.2000000000000000111 ) ;
#10363=FACE_OUTER_BOUND ( 'NONE', #9766, .T. ) ;
#10364=CARTESIAN_POINT ( 'NONE',  ( 21.00000000000000355, 0.000000000000000000, 0.000000000000000000 ) ) ;
#10390=FACE_OUTER_BOUND ( 'NONE', #501, .T. ) ;
#10397=VERTEX_POINT ( 'NONE', #6995 ) ;
#10404=VERTEX_POINT ( 'NONE', #3075 ) ;
#10406=CYLINDRICAL_SURFACE ( 'NONE', #8228, 2.500000000000000444 ) ;
#10436=DIRECTION ( 'NONE',  ( 0.000000000000000000, 0.000000000000000000, -1.000000000000000000 ) ) ;
#10442=EDGE_LOOP ( 'NONE', ( #7661, #1424, #4959, #5911, #1033 ) ) ;
#10457=ADVANCED_FACE ( 'NONE', ( #11045 ), #2507, .F. ) ;
#10458=PRODUCT ( 'socket head cap screw_iso_ISO 4762 M5 x 16 - 16N', 'socket head cap screw_iso_ISO 4762 M5 x 16 - 16N', '', ( #12352 ) ) ;
#10486=DIRECTION ( 'NONE',  ( 0.000000000000000000, -0.5000000000000009992, -0.8660254037844380415 ) ) ;
#10488=CARTESIAN_POINT ( 'NONE',  ( -31.74999999999995737, 0.000000000000000000, 4.250000000000000000 ) ) ;
#10500=ORIENTED_EDGE ( 'NONE', *, *, #10893, .T. ) ;
#10512=EDGE_CURVE ( 'NONE', #1340, #11798, #3380, .T. ) ;
#10516=CARTESIAN_POINT ( 'NONE',  ( 0.000000000000000000, 2.357898499370431722, -2.818925648462311528E-15 ) ) ;
#10526=ORIENTED_EDGE ( 'NONE', *, *, #6349, .F. ) ;
#10529=ORIENTED_EDGE ( 'NONE', *, *, #903, .T. ) ;
#10531=DIRECTION ( 'NONE',  ( -0.000000000000000000, 0.000000000000000000, 1.000000000000000000 ) ) ;
#10536=EDGE_CURVE ( 'NONE', #875, #10397, #8767, .T. ) ;
#10556=TOROIDAL_SURFACE ( 'NONE', #4388, 4.000000000000000000, 0.2500000000000000000 ) ;
#10586=EDGE_CURVE ( 'NONE', #8667, #12030, #9093, .T. ) ;
#10594=ORIENTED_EDGE ( 'NONE', *, *, #5321, .T. ) ;
#10608=ORIENTED_EDGE ( 'NONE', *, *, #4879, .T. ) ;
#10637=LINE ( 'NONE', #10516, #12054 ) ;
#10649=DIRECTION ( 'NONE',  ( -1.000000000000000000, -0.000000000000000000, -0.000000000000000000 ) ) ;
#10673=ADVANCED_FACE ( 'NONE', ( #3625 ), #11171, .T. ) ;
#10677=DIRECTION ( 'NONE',  ( 0.000000000000000000, 0.000000000000000000, 1.000000000000000000 ) ) ;
#10686=DIRECTION ( 'NONE',  ( 1.000000000000000000, 0.000000000000000000, 0.000000000000000000 ) ) ;
#10696=CARTESIAN_POINT ( 'NONE',  ( 0.000000000000000000, 0.000000000000000000, 0.000000000000000000 ) ) ;
#10704=AXIS2_PLACEMENT_3D ( 'NONE', #1805, #3984, #9394 ) ;
#10712=CARTESIAN_POINT ( 'NONE',  ( 0.000000000000000000, -2.357898499370432166, 3.035766082959412415E-15 ) ) ;
#10717=MECHANICAL_DESIGN_GEOMETRIC_PRESENTATION_REPRESENTATION('',(#10113),#11329);
#10721=ORIENTED_EDGE ( 'NONE', *, *, #4176, .T. ) ;
#10726=EDGE_LOOP ( 'NONE', ( #12023, #6687, #3360 ) ) ;
#10727=PLANE ( 'NONE',  #11176 ) ;
#10730=DIRECTION ( 'NONE',  ( -1.000000000000000000, -0.000000000000000000, -0.000000000000000000 ) ) ;
#10746=VERTEX_POINT ( 'NONE', #2938 ) ;
#10753=VECTOR ( 'NONE', #1085, 1000.000000000000000 ) ;
#10758=CARTESIAN_POINT ( 'NONE',  ( 5.200000000000002842, 3.306546357697854226E-16, 2.700000000000000622 ) ) ;
#10762=DIRECTION ( 'NONE',  ( 0.000000000000000000, -1.000000000000000000, 0.000000000000000000 ) ) ;
#10791=PLANE ( 'NONE',  #2663 ) ;
#10809=SURFACE_SIDE_STYLE ('',( #8809 ) ) ;
#10817=DIRECTION ( 'NONE',  ( 0.000000000000000000, 0.000000000000000000, 1.000000000000000000 ) ) ;
#10828=VECTOR ( 'NONE', #2384, 1000.000000000000000 ) ;
#10849=AXIS2_PLACEMENT_3D ( 'NONE', #2251, #6181, #6122 ) ;
#10870=AXIS2_PLACEMENT_3D ( 'NONE', #4492, #8344, #2679 ) ;
#10893=EDGE_CURVE ( 'NONE', #5925, #10404, #11911, .T. ) ;
#10911=VECTOR ( 'NONE', #5401, 1000.000000000000000 ) ;
#10917=ORIENTED_EDGE ( 'NONE', *, *, #11817, .T. ) ;
#10954=VECTOR ( 'NONE', #1546, 1000.000000000000000 ) ;
#10964=EDGE_CURVE ( 'NONE', #8921, #12045, #9972, .T. ) ;
#11001=EDGE_LOOP ( 'NONE', ( #1075, #2439, #10526 ) ) ;
#11003=UNCERTAINTY_MEASURE_WITH_UNIT (LENGTH_MEASURE( 1.000000000000000082E-05 ), #7995, 'distance_accuracy_value', 'NONE');
#11008=DIRECTION ( 'NONE',  ( 0.000000000000000000, -1.000000000000000000, 1.287488025362403787E-15 ) ) ;
#11010=DIRECTION ( 'NONE',  ( 0.000000000000000000, 0.000000000000000000, 1.000000000000000000 ) ) ;
#11024=EDGE_CURVE ( 'NONE', #4325, #4065, #5366, .T. ) ;
#11044=FACE_OUTER_BOUND ( 'NONE', #1088, .T. ) ;
#11045=FACE_OUTER_BOUND ( 'NONE', #6511, .T. ) ;
#11053=EDGE_CURVE ( 'NONE', #4065, #4325, #10130, .T. ) ;
#11080=LINE ( 'NONE', #7278, #3474 ) ;
#11088=LINE ( 'NONE', #8328, #8812 ) ;
#11107=PLANE ( 'NONE',  #8295 ) ;
#11108=CARTESIAN_POINT ( 'NONE',  ( 5.000000000000000888, 0.000000000000000000, 0.000000000000000000 ) ) ;
#11113=EDGE_CURVE ( 'NONE', #8974, #6884, #7353, .T. ) ;
#11114=EDGE_LOOP ( 'NONE', ( #912, #12091, #8637 ) ) ;
#11156=DIRECTION ( 'NONE',  ( -1.000000000000000000, -0.000000000000000000, -0.000000000000000000 ) ) ;
#11164=CARTESIAN_POINT ( 'NONE',  ( 2.500000000000000000, -1.178949249685214307, 2.042000000000001592 ) ) ;
#11167=( NAMED_UNIT ( * ) PLANE_ANGLE_UNIT ( ) SI_UNIT ( $, .RADIAN. ) );
#11168=CARTESIAN_POINT ( 'NONE',  ( -31.74999999999995737, 0.000000000000000000, 0.000000000000000000 ) ) ;
#11171=PLANE ( 'NONE',  #833 ) ;
#11176=AXIS2_PLACEMENT_3D ( 'NONE', #7858, #9847, #3943 ) ;
#11181=ORIENTED_EDGE ( 'NONE', *, *, #5390, .F. ) ;
#11212=EDGE_CURVE ( 'NONE', #10746, #11226, #12338, .T. ) ;
#11214=CARTESIAN_POINT ( 'NONE',  ( 0.2500000000000002220, 5.204748896376250699E-16, -4.250000000000000000 ) ) ;
#11221=DIRECTION ( 'NONE',  ( 0.000000000000000000, 0.000000000000000000, 1.000000000000000000 ) ) ;
#11226=VERTEX_POINT ( 'NONE', #11469 ) ;
#11238=ORIENTED_EDGE ( 'NONE', *, *, #8544, .T. ) ;
#11265=FACE_OUTER_BOUND ( 'NONE', #11114, .T. ) ;
#11273=VECTOR ( 'NONE', #960, 1000.000000000000000 ) ;
#11280=DIRECTION ( 'NONE',  ( 1.000000000000000000, 0.000000000000000000, 0.000000000000000000 ) ) ;
#11300=FACE_OUTER_BOUND ( 'NONE', #1616, .T. ) ;
#11322=DIRECTION ( 'NONE',  ( 0.000000000000000000, 0.000000000000000000, 1.000000000000000000 ) ) ;
#11329=( GEOMETRIC_REPRESENTATION_CONTEXT ( 3 ) GLOBAL_UNCERTAINTY_ASSIGNED_CONTEXT ( ( #1912 ) ) GLOBAL_UNIT_ASSIGNED_CONTEXT ( ( #3561, #11167, #10341 ) ) REPRESENTATION_CONTEXT ( 'NONE', 'WORKASPACE' ) );
#11368=ORIENTED_EDGE ( 'NONE', *, *, #903, .F. ) ;
#11373=FACE_OUTER_BOUND ( 'NONE', #4537, .T. ) ;
#11406=EDGE_LOOP ( 'NONE', ( #10319, #2428, #11238, #11641 ) ) ;
#11415=ORIENTED_EDGE ( 'NONE', *, *, #2349, .T. ) ;
#11424=EDGE_CURVE ( 'NONE', #10397, #875, #9750, .T. ) ;
#11469=CARTESIAN_POINT ( 'NONE',  ( 2.500000000000000000, 1.768423874527823791, 1.020999999999998353 ) ) ;
#11527=LINE ( 'NONE', #7590, #9031 ) ;
#11553=ORIENTED_EDGE ( 'NONE', *, *, #7340, .F. ) ;
#11564=ORIENTED_EDGE ( 'NONE', *, *, #6041, .T. ) ;
#11583=AXIS2_PLACEMENT_3D ( 'NONE', #8102, #3319, #4432 ) ;
#11593=AXIS2_PLACEMENT_3D ( 'NONE', #4217, #3222, #6904 ) ;
#11612=PRODUCT_DEFINITION ( 'UNKNOWN', '', #979, #11752 ) ;
#11620=CARTESIAN_POINT ( 'NONE',  ( 20.55500000000001748, 3.061616997868384127E-16, -2.500000000000000888 ) ) ;
#11626=CARTESIAN_POINT ( 'NONE',  ( 21.00000000000000355, 0.000000000000000000, 0.000000000000000000 ) ) ;
#11641=ORIENTED_EDGE ( 'NONE', *, *, #1804, .F. ) ;
#11668=ORIENTED_EDGE ( 'NONE', *, *, #5843, .T. ) ;
#11673=EDGE_LOOP ( 'NONE', ( #6329, #3495, #9604 ) ) ;
#11696=DIRECTION ( 'NONE',  ( 1.000000000000000000, 0.000000000000000000, 0.000000000000000000 ) ) ;
#11711=EDGE_LOOP ( 'NONE', ( #11668, #12238, #3172 ) ) ;
#11715=CARTESIAN_POINT ( 'NONE',  ( 2.500000000000000000, -1.768423874527823569, 1.021000000000002350 ) ) ;
#11722=DIRECTION ( 'NONE',  ( -1.000000000000000000, -0.000000000000000000, -0.000000000000000000 ) ) ;
#11748=ADVANCED_FACE ( 'NONE', ( #7231 ), #5551, .T. ) ;
#11752=PRODUCT_DEFINITION_CONTEXT ( 'detailed design', #3826, 'design' ) ;
#11766=AXIS2_PLACEMENT_3D ( 'NONE', #6221, #607, #6967 ) ;
#11780=FACE_OUTER_BOUND ( 'NONE', #11406, .T. ) ;
#11798=VERTEX_POINT ( 'NONE', #12100 ) ;
#11817=EDGE_CURVE ( 'NONE', #10746, #7164, #4541, .T. ) ;
#11841=CIRCLE ( 'NONE', #2275, 4.000000000000000000 ) ;
#11858=ORIENTED_EDGE ( 'NONE', *, *, #9434, .T. ) ;
#11881=CARTESIAN_POINT ( 'NONE',  ( 2.500000000000000000, 2.357898499370431722, -2.818925648462311528E-15 ) ) ;
#11883=CARTESIAN_POINT ( 'NONE',  ( 4.999999999999997335, 0.000000000000000000, 4.250000000000000000 ) ) ;
#11886=STYLED_ITEM ( 'NONE', ( #2332 ), #8859 ) ;
#11898=CARTESIAN_POINT ( 'NONE',  ( 0.2500000000000002220, 0.000000000000000000, 4.000000000000000000 ) ) ;
#11903=CARTESIAN_POINT ( 'NONE',  ( 0.000000000000000000, -1.178949249685214307, 2.042000000000001592 ) ) ;
#11911=LINE ( 'NONE', #6294, #3612 ) ;
#11919=EDGE_CURVE ( 'NONE', #3768, #1236, #3788, .T. ) ;
#11933=ORIENTED_EDGE ( 'NONE', *, *, #1240, .F. ) ;
#11953=LINE ( 'NONE', #3224, #5906 ) ;
#11959=DIRECTION ( 'NONE',  ( 0.000000000000000000, 0.000000000000000000, 1.000000000000000000 ) ) ;
#11962=AXIS2_PLACEMENT_3D ( 'NONE', #10364, #2761, #3578 ) ;
#11970=CARTESIAN_POINT ( 'NONE',  ( 0.000000000000000000, 0.000000000000000000, 4.000000000000000000 ) ) ;
#11974=AXIS2_PLACEMENT_3D ( 'NONE', #11108, #9852, #2445 ) ;
#11987=CIRCLE ( 'NONE', #2815, 2.041999999999999815 ) ;
#11999=CARTESIAN_POINT ( 'NONE',  ( -31.74999999999995737, 5.204748896376250699E-16, -4.250000000000000000 ) ) ;
#12023=ORIENTED_EDGE ( 'NONE', *, *, #3762, .T. ) ;
#12030=VERTEX_POINT ( 'NONE', #5854 ) ;
#12037=VECTOR ( 'NONE', #8605, 999.9999999999997726 ) ;
#12045=VERTEX_POINT ( 'NONE', #3163 ) ;
#12051=ORIENTED_EDGE ( 'NONE', *, *, #1773, .F. ) ;
#12054=VECTOR ( 'NONE', #987, 1000.000000000000000 ) ;
#12075=EDGE_CURVE ( 'NONE', #6884, #11798, #5229, .T. ) ;
#12080=ADVANCED_FACE ( 'NONE', ( #11780 ), #10556, .T. ) ;
#12089=AXIS2_PLACEMENT_3D ( 'NONE', #1768, #7505, #5521 ) ;
#12091=ORIENTED_EDGE ( 'NONE', *, *, #1222, .T. ) ;
#12100=CARTESIAN_POINT ( 'NONE',  ( 0.000000000000000000, 1.178949249685217415, 2.041999999999998483 ) ) ;
#12112=DIRECTION ( 'NONE',  ( 0.000000000000000000, 0.000000000000000000, 1.000000000000000000 ) ) ;
#12151=FACE_OUTER_BOUND ( 'NONE', #2006, .T. ) ;
#12157=ADVANCED_FACE ( 'NONE', ( #2411 ), #10361, .F. ) ;
#12159=ORIENTED_EDGE ( 'NONE', *, *, #956, .F. ) ;
#12181=VECTOR ( 'NONE', #4780, 1000.000000000000000 ) ;
#12196=ORIENTED_EDGE ( 'NONE', *, *, #11024, .F. ) ;
#12211=ORIENTED_EDGE ( 'NONE', *, *, #3717, .T. ) ;
#12218=CARTESIAN_POINT ( 'NONE',  ( 2.500000000000000000, -1.178949249685214307, 2.042000000000001592 ) ) ;
#12232=PRESENTATION_STYLE_ASSIGNMENT (( #8223 ) ) ;
#12238=ORIENTED_EDGE ( 'NONE', *, *, #5321, .F. ) ;
#12246=AXIS2_PLACEMENT_3D ( 'NONE', #9634, #6596, #6720 ) ;
#12264=DIRECTION ( 'NONE',  ( 0.000000000000000000, 0.000000000000000000, 1.000000000000000000 ) ) ;
#12283=AXIS2_PLACEMENT_3D ( 'NONE', #8500, #5467, #12264 ) ;
#12308=CARTESIAN_POINT ( 'NONE',  ( 21.00000000000000355, 0.000000000000000000, 2.055000000000000160 ) ) ;
#12338=LINE ( 'NONE', #4853, #384 ) ;
#12352=PRODUCT_CONTEXT ( 'NONE', #8674, 'mechanical' ) ;
ENDSEC;
END-ISO-10303-21;
